ISO-10303-21;
HEADER;
/* Generated by software containing ST-Developer
 * from STEP Tools, Inc. (www.steptools.com) 
 */

FILE_DESCRIPTION(
/* description */ ('PAT-003'),
/* implementation_level */ '2;1');

FILE_NAME(
/* name */ 'Flat Washer - M8.step',
/* time_stamp */ '2026-10-29T15:45:40-07:00',
/* author */ (''),
/* organization */ (''),
/* preprocessor_version */ 'ST-DEVELOPER v20.2',
/* originating_system */ 'Autodesk Translation Framework v15.17.0.0',
/* authorisation */ '');

FILE_SCHEMA (('AUTOMOTIVE_DESIGN { 1 0 10303 214 3 1 1 }'));
ENDSEC;

DATA;
#10=MECHANICAL_DESIGN_GEOMETRIC_PRESENTATION_REPRESENTATION('',(#156),#5761);
#132=SHAPE_REPRESENTATION_RELATIONSHIP('SRR','None',#5827,#144);
#144=ADVANCED_BREP_SHAPE_REPRESENTATION('',(#166),#5758);
#156=STYLED_ITEM('',(#5956),#166);
#166=MANIFOLD_SOLID_BREP('Body1',#3332);
#199=FACE_BOUND('',#711,.T.);
#200=FACE_BOUND('',#713,.T.);
#322=PLANE('',#3701);
#323=PLANE('',#3702);
#491=FACE_OUTER_BOUND('',#708,.T.);
#492=FACE_OUTER_BOUND('',#709,.T.);
#493=FACE_OUTER_BOUND('',#710,.T.);
#494=FACE_OUTER_BOUND('',#712,.T.);
#708=EDGE_LOOP('',(#2918,#2919,#2920,#2921));
#709=EDGE_LOOP('',(#2922,#2923,#2924,#2925));
#710=EDGE_LOOP('',(#2926));
#711=EDGE_LOOP('',(#2927));
#712=EDGE_LOOP('',(#2928));
#713=EDGE_LOOP('',(#2929));
#1032=LINE('',#5506,#1354);
#1033=LINE('',#5512,#1355);
#1354=VECTOR('',#4525,0.42);
#1355=VECTOR('',#4532,0.8);
#1458=CIRCLE('',#3696,0.42);
#1459=CIRCLE('',#3697,0.42);
#1460=CIRCLE('',#3699,0.8);
#1461=CIRCLE('',#3700,0.8);
#1722=VERTEX_POINT('',#5503);
#1723=VERTEX_POINT('',#5505);
#1724=VERTEX_POINT('',#5509);
#1725=VERTEX_POINT('',#5511);
#2130=EDGE_CURVE('',#1722,#1722,#1458,.T.);
#2131=EDGE_CURVE('',#1722,#1723,#1032,.T.);
#2132=EDGE_CURVE('',#1723,#1723,#1459,.T.);
#2133=EDGE_CURVE('',#1724,#1724,#1460,.T.);
#2134=EDGE_CURVE('',#1724,#1725,#1033,.T.);
#2135=EDGE_CURVE('',#1725,#1725,#1461,.T.);
#2918=ORIENTED_EDGE('',*,*,#2130,.F.);
#2919=ORIENTED_EDGE('',*,*,#2131,.T.);
#2920=ORIENTED_EDGE('',*,*,#2132,.T.);
#2921=ORIENTED_EDGE('',*,*,#2131,.F.);
#2922=ORIENTED_EDGE('',*,*,#2133,.F.);
#2923=ORIENTED_EDGE('',*,*,#2134,.T.);
#2924=ORIENTED_EDGE('',*,*,#2135,.T.);
#2925=ORIENTED_EDGE('',*,*,#2134,.F.);
#2926=ORIENTED_EDGE('',*,*,#2133,.T.);
#2927=ORIENTED_EDGE('',*,*,#2130,.T.);
#2928=ORIENTED_EDGE('',*,*,#2135,.F.);
#2929=ORIENTED_EDGE('',*,*,#2132,.F.);
#3118=CYLINDRICAL_SURFACE('',#3695,0.42);
#3119=CYLINDRICAL_SURFACE('',#3698,0.8);
#3284=ADVANCED_FACE('',(#491),#3118,.F.);
#3285=ADVANCED_FACE('',(#492),#3119,.T.);
#3286=ADVANCED_FACE('',(#493,#199),#322,.T.);
#3287=ADVANCED_FACE('',(#494,#200),#323,.F.);
#3332=CLOSED_SHELL('',(#3284,#3285,#3286,#3287));
#3694=AXIS2_PLACEMENT_3D('',#5501,#4519,#4520);
#3695=AXIS2_PLACEMENT_3D('',#5502,#4521,#4522);
#3696=AXIS2_PLACEMENT_3D('',#5504,#4523,#4524);
#3697=AXIS2_PLACEMENT_3D('',#5507,#4526,#4527);
#3698=AXIS2_PLACEMENT_3D('',#5508,#4528,#4529);
#3699=AXIS2_PLACEMENT_3D('',#5510,#4530,#4531);
#3700=AXIS2_PLACEMENT_3D('',#5513,#4533,#4534);
#3701=AXIS2_PLACEMENT_3D('',#5514,#4535,#4536);
#3702=AXIS2_PLACEMENT_3D('',#5515,#4537,#4538);
#4519=DIRECTION('axis',(0.,0.,1.));
#4520=DIRECTION('refdir',(1.,0.,0.));
#4521=DIRECTION('center_axis',(0.,1.,0.));
#4522=DIRECTION('ref_axis',(1.,0.,0.));
#4523=DIRECTION('center_axis',(0.,-1.,0.));
#4524=DIRECTION('ref_axis',(1.,0.,0.));
#4525=DIRECTION('',(0.,-1.,0.));
#4526=DIRECTION('center_axis',(0.,-1.,0.));
#4527=DIRECTION('ref_axis',(1.,0.,0.));
#4528=DIRECTION('center_axis',(0.,1.,0.));
#4529=DIRECTION('ref_axis',(1.,0.,0.));
#4530=DIRECTION('center_axis',(0.,1.,0.));
#4531=DIRECTION('ref_axis',(1.,0.,0.));
#4532=DIRECTION('',(0.,-1.,0.));
#4533=DIRECTION('center_axis',(0.,1.,0.));
#4534=DIRECTION('ref_axis',(1.,0.,0.));
#4535=DIRECTION('center_axis',(0.,1.,0.));
#4536=DIRECTION('ref_axis',(1.,0.,0.));
#4537=DIRECTION('center_axis',(0.,1.,0.));
#4538=DIRECTION('ref_axis',(1.,0.,0.));
#5501=CARTESIAN_POINT('',(0.,0.,0.));
#5502=CARTESIAN_POINT('Origin',(0.,0.,0.));
#5503=CARTESIAN_POINT('',(-0.42,0.16,5.14351655641888E-17));
#5504=CARTESIAN_POINT('Origin',(0.,0.16,0.));
#5505=CARTESIAN_POINT('',(-0.42,0.,5.14351655641888E-17));
#5506=CARTESIAN_POINT('',(-0.42,0.,5.14351655641888E-17));
#5507=CARTESIAN_POINT('Origin',(0.,0.,0.));
#5508=CARTESIAN_POINT('Origin',(0.,0.,0.));
#5509=CARTESIAN_POINT('',(-0.8,0.16,9.79717439317883E-17));
#5510=CARTESIAN_POINT('Origin',(0.,0.16,0.));
#5511=CARTESIAN_POINT('',(-0.8,0.,9.79717439317883E-17));
#5512=CARTESIAN_POINT('',(-0.8,0.,9.79717439317883E-17));
#5513=CARTESIAN_POINT('Origin',(0.,0.,0.));
#5514=CARTESIAN_POINT('Origin',(0.,0.16,0.));
#5515=CARTESIAN_POINT('Origin',(0.,0.,0.));
#5742=UNCERTAINTY_MEASURE_WITH_UNIT(LENGTH_MEASURE(0.001),#5762,
'DISTANCE_ACCURACY_VALUE',
'Maximum model space distance between geometric entities at asserted c
onnectivities');
#5745=UNCERTAINTY_MEASURE_WITH_UNIT(LENGTH_MEASURE(0.001),#5762,
'DISTANCE_ACCURACY_VALUE',
'Maximum model space distance between geometric entities at asserted c
onnectivities');
#5758=(
GEOMETRIC_REPRESENTATION_CONTEXT(3)
GLOBAL_UNCERTAINTY_ASSIGNED_CONTEXT((#5742))
GLOBAL_UNIT_ASSIGNED_CONTEXT((#5762,#5764,#5765))
REPRESENTATION_CONTEXT('','3D')
);
#5761=(
GEOMETRIC_REPRESENTATION_CONTEXT(3)
GLOBAL_UNCERTAINTY_ASSIGNED_CONTEXT((#5745))
GLOBAL_UNIT_ASSIGNED_CONTEXT((#5762,#5764,#5765))
REPRESENTATION_CONTEXT('','3D')
);
#5762=(
LENGTH_UNIT()
NAMED_UNIT(*)
SI_UNIT(.CENTI.,.METRE.)
);
#5764=(
NAMED_UNIT(*)
PLANE_ANGLE_UNIT()
SI_UNIT($,.RADIAN.)
);
#5765=(
NAMED_UNIT(*)
SI_UNIT($,.STERADIAN.)
SOLID_ANGLE_UNIT()
);
#5778=SHAPE_DEFINITION_REPRESENTATION(#5793,#5827);
#5793=PRODUCT_DEFINITION_SHAPE('',$,#5843);
#5827=SHAPE_REPRESENTATION('',(#3694),#5758);
#5830=PRODUCT_DEFINITION_CONTEXT('part definition',#5877,'design');
#5843=PRODUCT_DEFINITION('Flat Washer - M8','Flat Washer - M8',#5858,#5830);
#5858=PRODUCT_DEFINITION_FORMATION('',$,#5891);
#5877=APPLICATION_CONTEXT(
'Core Data for Automotive Mechanical Design Process');
#5878=PRODUCT_CONTEXT('part definition',#5877,'mechanical');
#5891=PRODUCT('Flat Washer - M8','Flat Washer - M8','Flat Washer - M8',
(#5878));
#5950=COLOUR_RGB('Black',0.12,0.14,0.17);
#5951=FILL_AREA_STYLE_COLOUR('',#5950);
#5952=FILL_AREA_STYLE('',(#5951));
#5953=SURFACE_STYLE_FILL_AREA(#5952);
#5954=SURFACE_SIDE_STYLE('',(#5953));
#5955=SURFACE_STYLE_USAGE(.BOTH.,#5954);
#5956=PRESENTATION_STYLE_ASSIGNMENT((#5955));
ENDSEC;
END-ISO-10303-21;
